ISO-10303-21;
HEADER;
FILE_DESCRIPTION (('STEP AP214'),
    '1' );
FILE_NAME ('Bolt.step',
    '2026-10-23T20:35:44',
    ( '' ),
    ( '' ),
    'SwSTEP 2.0',
    'SolidWorks 2025',
    '' );
FILE_SCHEMA (( 'AUTOMOTIVE_DESIGN' ));
ENDSEC;

DATA;
#2=CARTESIAN_POINT ( 'NONE',  ( 1.172031980416358365, -0.1441408498666779114, 0.9737261629585141076 ) ) ;
#10=VERTEX_POINT ( 'NONE', #4360 ) ;
#25=DIRECTION ( 'NONE',  ( 0.000000000000000000, 0.000000000000000000, -1.000000000000000000 ) ) ;
#38=CARTESIAN_POINT ( 'NONE',  ( 0.8794895096619267383, -0.2118599820681134061, 0.9611874069187010816 ) ) ;
#120=ORIENTED_EDGE ( 'NONE', *, *, #5116, .T. ) ;
#141=PRODUCT ( 'Bolt', 'Bolt', '', ( #5415 ) ) ;
#143=CARTESIAN_POINT ( 'NONE',  ( 0.7480314960629923515, 1.205359478595430764E-16, -0.9842519685039370358 ) ) ;
#154=VECTOR ( 'NONE', #737, 39.37007874015748143 ) ;
#176=SHAPE_DEFINITION_REPRESENTATION ( #334, #2147 ) ;
#191=B_SPLINE_CURVE_WITH_KNOTS ( 'NONE', 3,
 ( #3189, #3844, #2647, #6068, #7236, #2009, #5539, #6708, #896, #7196, #1384, #1453, #4340, #3875, #972, #4412, #4297, #327, #4989, #7308, #2085, #1493, #6175, #930, #3260, #3299, #5650, #6636, #3380, #1719, #6358, #3962, #2195, #6932, #7494, #2869, #5212, #3419, #6326, #1574 ),
 .UNSPECIFIED., .F., .F.,
 ( 4, 2, 2, 2, 2, 2, 2, 2, 2, 2, 2, 2, 2, 2, 2, 2, 2, 2, 2, 4 ),
 ( 0.01882766236946021784, 0.02000407617178198011, 0.02118048997410373890, 0.02176869687526461830, 0.02235690377642549770, 0.02353331757874724955, 0.02470973138106900141, 0.02588614518339075327, 0.02706255898571250512, 0.02765076588687337758, 0.02823897278803425004, 0.02941538659035599496, 0.03059180039267773293, 0.03176821419499947785, 0.03235642109616034684, 0.03294462799732121583, 0.03412104179964296768, 0.03529745560196471260, 0.03647386940428645752, 0.03765028320660820244 ),
 .UNSPECIFIED. ) ;
#212=PRODUCT_DEFINITION_FORMATION_WITH_SPECIFIED_SOURCE ( 'ANY', '', #141, .NOT_KNOWN. ) ;
#230=LINE ( 'NONE', #5471, #3282 ) ;
#260=CARTESIAN_POINT ( 'NONE',  ( 0.8791862816395774605, -0.2121393407445530399, -0.9611380397500175476 ) ) ;
#296=( GEOMETRIC_REPRESENTATION_CONTEXT ( 3 ) GLOBAL_UNCERTAINTY_ASSIGNED_CONTEXT ( ( #7477 ) ) GLOBAL_UNIT_ASSIGNED_CONTEXT ( ( #4575, #4535, #6833 ) ) REPRESENTATION_CONTEXT ( 'NONE', 'WORKASPACE' ) );
#297=EDGE_LOOP ( 'NONE', ( #6707, #7218, #922, #3341 ) ) ;
#327=CARTESIAN_POINT ( 'NONE',  ( 0.9454567723360981502, 0.2331403729576253803, 0.9562426076827387211 ) ) ;
#334=PRODUCT_DEFINITION_SHAPE ( 'NONE', 'NONE',  #1953 ) ;
#338=CARTESIAN_POINT ( 'NONE',  ( 0.8465112843344620996, 0.1920587529112295633, -0.9653415754825105388 ) ) ;
#359=DIRECTION ( 'NONE',  ( 0.000000000000000000, 0.000000000000000000, -1.000000000000000000 ) ) ;
#372=CARTESIAN_POINT ( 'NONE',  ( 21.65354330708661479, 0.000000000000000000, 0.4921259842519685179 ) ) ;
#375=CARTESIAN_POINT ( 'NONE',  ( 0.7601524118086268045, 0.07627561187719542057, -0.9813965260305658189 ) ) ;
#387=EDGE_CURVE ( 'NONE', #3423, #6545, #3883, .T. ) ;
#414=CARTESIAN_POINT ( 'NONE',  ( 0.9530933633567026941, -0.2342849080887553226, -0.9559618965236083010 ) ) ;
#417=CARTESIAN_POINT ( 'NONE',  ( 1.140380516255546706, 0.1779313096650642356, -0.9680979248264950376 ) ) ;
#418=CARTESIAN_POINT ( 'NONE',  ( 0.000000000000000000, 0.000000000000000000, 0.000000000000000000 ) ) ;
#436=DIMENSIONAL_EXPONENTS ( 1.000000000000000000, 0.000000000000000000, 0.000000000000000000, 0.000000000000000000, 0.000000000000000000, 0.000000000000000000, 0.000000000000000000 ) ;
#455=( LENGTH_UNIT ( ) NAMED_UNIT ( * ) SI_UNIT ( $, .METRE. ) );
#458=( LENGTH_UNIT ( ) NAMED_UNIT ( * ) SI_UNIT ( $, .METRE. ) );
#470=VECTOR ( 'NONE', #3256, 39.37007874015748143 ) ;
#491=EDGE_LOOP ( 'NONE', ( #3148, #2683 ) ) ;
#517=CARTESIAN_POINT ( 'NONE',  ( 0.8226608724162054465, -0.1724771829768798059, 0.9690378908208601150 ) ) ;
#538=PLANE ( 'NONE',  #6985 ) ;
#549=CARTESIAN_POINT ( 'NONE',  ( 1.196439825128248202, -0.1049569639594290504, 0.9787451009560118598 ) ) ;
#590=CIRCLE ( 'NONE', #2658, 0.4921259842519685179 ) ;
#599=CYLINDRICAL_SURFACE ( 'NONE', #4915, 0.4921259842519685179 ) ;
#623=ORIENTED_EDGE ( 'NONE', *, *, #4625, .F. ) ;
#645=CARTESIAN_POINT ( 'NONE',  ( 21.65354330708661479, 0.000000000000000000, 0.000000000000000000 ) ) ;
#646=DIRECTION ( 'NONE',  ( 1.000000000000000000, 0.000000000000000000, 0.000000000000000000 ) ) ;
#649=ORIENTED_EDGE ( 'NONE', *, *, #1537, .F. ) ;
#693=CARTESIAN_POINT ( 'NONE',  ( 0.7499405322945513763, -0.03096673178975459240, 0.9837952645051013523 ) ) ;
#720=AXIS2_PLACEMENT_3D ( 'NONE', #645, #4729, #2481 ) ;
#721=FACE_OUTER_BOUND ( 'NONE', #7140, .T. ) ;
#731=CARTESIAN_POINT ( 'NONE',  ( 1.968503937007874072, 0.000000000000000000, 0.9842519685039370358 ) ) ;
#732=CARTESIAN_POINT ( 'NONE',  ( 1.968503937007874072, 0.000000000000000000, 0.000000000000000000 ) ) ;
#737=DIRECTION ( 'NONE',  ( -0.000000000000000000, -0.000000000000000000, 1.000000000000000000 ) ) ;
#744=EDGE_CURVE ( 'NONE', #6545, #6588, #776, .T. ) ;
#769=CARTESIAN_POINT ( 'NONE',  ( 21.65354330708661479, 0.000000000000000000, 0.000000000000000000 ) ) ;
#776=LINE ( 'NONE', #5984, #154 ) ;
#790=CARTESIAN_POINT ( 'NONE',  ( 1.207998888640173130, 0.07614347099379424610, -0.9813305615101511892 ) ) ;
#795=CARTESIAN_POINT ( 'NONE',  ( 21.65354330708661479, 6.026805113914139867E-17, -0.4921259842519685179 ) ) ;
#820=LINE ( 'NONE', #3731, #6144 ) ;
#828=CARTESIAN_POINT ( 'NONE',  ( 0.9763767025864577009, -0.2362177056199707692, -0.9554858099749828915 ) ) ;
#831=DIRECTION ( 'NONE',  ( -1.000000000000000000, -0.000000000000000000, -0.000000000000000000 ) ) ;
#891=EDGE_CURVE ( 'NONE', #6362, #4753, #7466, .T. ) ;
#896=CARTESIAN_POINT ( 'NONE',  ( 0.7836514762968587178, 0.1249763776241986785, 0.9763066675542205752 ) ) ;
#922=ORIENTED_EDGE ( 'NONE', *, *, #3553, .T. ) ;
#926=CARTESIAN_POINT ( 'NONE',  ( 1.968503937007874072, 0.000000000000000000, 0.9842519685039370358 ) ) ;
#927=ORIENTED_EDGE ( 'NONE', *, *, #387, .T. ) ;
#930=CARTESIAN_POINT ( 'NONE',  ( 1.045446081760740942, 0.2286795840550674142, 0.9573229298165720769 ) ) ;
#948=CARTESIAN_POINT ( 'NONE',  ( 1.968503937007874072, 6.026805113914139867E-17, -0.4921259842519685179 ) ) ;
#972=CARTESIAN_POINT ( 'NONE',  ( 0.8791862816395774605, 0.2121393407445530399, 0.9611380397500175476 ) ) ;
#978=CARTESIAN_POINT ( 'NONE',  ( 0.9227869198894881331, -0.2286038407206694989, -0.9573410596537438311 ) ) ;
#1004=DIRECTION ( 'NONE',  ( 1.000000000000000000, 0.000000000000000000, 0.000000000000000000 ) ) ;
#1028=EDGE_CURVE ( 'NONE', #6588, #4456, #3758, .T. ) ;
#1039=EDGE_LOOP ( 'NONE', ( #649, #2721, #2871, #3146 ) ) ;
#1041=CARTESIAN_POINT ( 'NONE',  ( 0.9998202959290236613, -0.2362140621487221481, 0.9554867107345892396 ) ) ;
#1053=CARTESIAN_POINT ( 'NONE',  ( 0.8403423717953923955, 0.1874820019069840249, -0.9662438517680175254 ) ) ;
#1071=CARTESIAN_POINT ( 'NONE',  ( 1.162092266633492077, -0.1562322077656922159, 0.9718357064180906946 ) ) ;
#1122=CARTESIAN_POINT ( 'NONE',  ( 21.65354330708661479, 0.000000000000000000, 0.000000000000000000 ) ) ;
#1134=CARTESIAN_POINT ( 'NONE',  ( 1.128523761465410891, -0.1876879802734073011, 0.9662312300142489319 ) ) ;
#1148=ORIENTED_EDGE ( 'NONE', *, *, #1028, .T. ) ;
#1151=DIRECTION ( 'NONE',  ( 0.000000000000000000, 0.000000000000000000, -1.000000000000000000 ) ) ;
#1189=ADVANCED_FACE ( 'NONE', ( #6547 ), #3490, .T. ) ;
#1201=CARTESIAN_POINT ( 'NONE',  ( 21.65354330708661479, 0.000000000000000000, 0.000000000000000000 ) ) ;
#1209=CARTESIAN_POINT ( 'NONE',  ( 0.7480314960629923515, 1.544184662414706467E-22, 0.9842519685039370358 ) ) ;
#1248=VERTEX_POINT ( 'NONE', #948 ) ;
#1288=CARTESIAN_POINT ( 'NONE',  ( 0.7719899816204534027, -0.1048018568659492278, 0.9787612993317383880 ) ) ;
#1291=DIRECTION ( 'NONE',  ( 1.000000000000000000, 0.000000000000000000, 0.000000000000000000 ) ) ;
#1292=FACE_OUTER_BOUND ( 'NONE', #5354, .T. ) ;
#1315=CARTESIAN_POINT ( 'NONE',  ( 1.205350347085700102, 0.08351947907094880996, -0.9807282671443031674 ) ) ;
#1327=DIRECTION ( 'NONE',  ( 1.000000000000000000, 0.000000000000000000, 0.000000000000000000 ) ) ;
#1330=CARTESIAN_POINT ( 'NONE',  ( 0.7511002112796222319, -0.03873617871155973086, 0.9835188775901014813 ) ) ;
#1354=AXIS2_PLACEMENT_3D ( 'NONE', #769, #3136, #4515 ) ;
#1372=CARTESIAN_POINT ( 'NONE',  ( 0.7556634140584972403, -0.06154568813258620014, 0.9824437959648022467 ) ) ;
#1384=CARTESIAN_POINT ( 'NONE',  ( 0.8062609481994166272, 0.1560654929534785462, 0.9718629971449804783 ) ) ;
#1391=CARTESIAN_POINT ( 'NONE',  ( 1.102581283201567564, -0.2050316615124324060, -0.9626998336838916703 ) ) ;
#1425=ADVANCED_FACE ( 'NONE', ( #3432, #1665 ), #7437, .T. ) ;
#1450=LINE ( 'NONE', #4906, #6203 ) ;
#1453=CARTESIAN_POINT ( 'NONE',  ( 0.8280287984149673486, 0.1778526427332735582, 0.9681128863842415333 ) ) ;
#1459=CARTESIAN_POINT ( 'NONE',  ( 1.145762533245342940, -0.1725491722722915233, -0.9690247371578599722 ) ) ;
#1461=CARTESIAN_POINT ( 'NONE',  ( 1.102718734937994105, 0.2049554913489460561, -0.9627163727494573164 ) ) ;
#1493=CARTESIAN_POINT ( 'NONE',  ( 0.9997522001112967294, 0.2362259618796917759, 0.9554837688155867204 ) ) ;
#1505=CARTESIAN_POINT ( 'NONE',  ( 0.8226608724162054465, 0.1724771829768798059, -0.9690378908208601150 ) ) ;
#1506=VECTOR ( 'NONE', #831, 39.37007874015748143 ) ;
#1537=EDGE_CURVE ( 'NONE', #1603, #6545, #2213, .T. ) ;
#1541=CARTESIAN_POINT ( 'NONE',  ( 0.9685300475558180633, -0.2358242948353262147, -0.9555833128140062138 ) ) ;
#1544=CARTESIAN_POINT ( 'NONE',  ( 1.089060247968624440, 0.2122540722833457794, -0.9611122372014845316 ) ) ;
#1558=MANIFOLD_SOLID_BREP ( 'Boss-Extrude2', #7369 ) ;
#1574=CARTESIAN_POINT ( 'NONE',  ( 1.220472440944881720, -1.984939871850715226E-17, 0.9842519685039370358 ) ) ;
#1603=VERTEX_POINT ( 'NONE', #5079 ) ;
#1609=ORIENTED_EDGE ( 'NONE', *, *, #6825, .F. ) ;
#1610=CARTESIAN_POINT ( 'NONE',  ( 0.8403423717953923955, -0.1874820019069840249, 0.9662438517680175254 ) ) ;
#1611=CARTESIAN_POINT ( 'NONE',  ( 21.65354330708661479, 0.000000000000000000, 0.4921259842519685179 ) ) ;
#1648=CARTESIAN_POINT ( 'NONE',  ( 0.8592737258235019215, -0.2005978551774719454, 0.9636033532647499955 ) ) ;
#1664=( CONVERSION_BASED_UNIT ( 'INCH', #4579 ) LENGTH_UNIT ( ) NAMED_UNIT ( #2768 ) );
#1665=FACE_OUTER_BOUND ( 'NONE', #5827, .T. ) ;
#1670=EDGE_CURVE ( 'NONE', #1248, #10, #6582, .T. ) ;
#1682=CIRCLE ( 'NONE', #2408, 0.9842519685039370358 ) ;
#1719=CARTESIAN_POINT ( 'NONE',  ( 1.140074190135267118, 0.1777047106289595946, 0.9680897379949867654 ) ) ;
#1764=CARTESIAN_POINT ( 'NONE',  ( 0.7480314960629923515, 1.205359478595430764E-16, -0.9842519685039370358 ) ) ;
#1766=ORIENTED_EDGE ( 'NONE', *, *, #3978, .T. ) ;
#1777=DIRECTION ( 'NONE',  ( 1.000000000000000000, 0.000000000000000000, 0.000000000000000000 ) ) ;
#1780=DIRECTION ( 'NONE',  ( -1.000000000000000000, -0.000000000000000000, -0.000000000000000000 ) ) ;
#1853=AXIS2_PLACEMENT_3D ( 'NONE', #6813, #3914, #359 ) ;
#1860=CARTESIAN_POINT ( 'NONE',  ( 1.214400861842334090, 0.05376942629958520597, -0.9828113691670130603 ) ) ;
#1861=VECTOR ( 'NONE', #1780, 39.37007874015748143 ) ;
#1899=CARTESIAN_POINT ( 'NONE',  ( 0.7601650273709252836, -0.07630400123961592063, -0.9813937435533869325 ) ) ;
#1902=CARTESIAN_POINT ( 'NONE',  ( 1.189177986357916605, 0.1185041968903534776, -0.9771775582510943137 ) ) ;
#1953=PRODUCT_DEFINITION ( 'UNKNOWN', '', #212, #5961 ) ;
#1971=CARTESIAN_POINT ( 'NONE',  ( 0.9842519685039370358, 0.000000000000000000, -1.377952755905512028 ) ) ;
#1978=CARTESIAN_POINT ( 'NONE',  ( 0.9079010304997725544, -0.2240813082648737964, -0.9584242268600799974 ) ) ;
#2009=CARTESIAN_POINT ( 'NONE',  ( 0.7690174846032691303, 0.09763972085202782258, 0.9794230103293317669 ) ) ;
#2010=ORIENTED_EDGE ( 'NONE', *, *, #3978, .F. ) ;
#2012=CYLINDRICAL_SURFACE ( 'NONE', #2815, 0.2362204724409446843 ) ;
#2078=ORIENTED_EDGE ( 'NONE', *, *, #2987, .F. ) ;
#2085=CARTESIAN_POINT ( 'NONE',  ( 0.9763767025864577009, 0.2362177056199707692, 0.9554858099749828915 ) ) ;
#2099=ORIENTED_EDGE ( 'NONE', *, *, #891, .F. ) ;
#2119=VERTEX_POINT ( 'NONE', #795 ) ;
#2134=DIRECTION ( 'NONE',  ( 0.000000000000000000, 0.000000000000000000, 1.000000000000000000 ) ) ;
#2147=SHAPE_REPRESENTATION ( 'Bolt', ( #5166 ), #3072 ) ;
#2168=ADVANCED_FACE ( 'NONE', ( #721 ), #6650, .T. ) ;
#2187=ORIENTED_EDGE ( 'NONE', *, *, #5635, .T. ) ;
#2195=CARTESIAN_POINT ( 'NONE',  ( 1.171887040486664588, 0.1443386382778019672, 0.9736977440596933375 ) ) ;
#2206=CARTESIAN_POINT ( 'NONE',  ( 1.162092266633492077, 0.1562322077656922159, -0.9718357064180906946 ) ) ;
#2213=B_SPLINE_CURVE_WITH_KNOTS ( 'NONE', 3,
 ( #143, #4806, #7132, #7166, #1899, #4230, #3660, #5425, #4423, #6074, #7203, #2697, #6795, #3850, #260, #1978, #978, #6714, #414, #1541, #828, #4383, #2583, #7357, #6183, #6149, #1391, #6108, #5582, #4921, #1459, #7278, #7247, #3268, #6752, #5620, #6642, #3197, #3889, #4346 ),
 .UNSPECIFIED., .F., .F.,
 ( 4, 2, 2, 2, 2, 2, 2, 2, 2, 2, 2, 2, 2, 2, 2, 2, 2, 2, 2, 4 ),
 ( 0.01882766236946021784, 0.02000407617178198011, 0.02118048997410373890, 0.02176869687526461830, 0.02235690377642549770, 0.02353331757874724955, 0.02470973138106900141, 0.02588614518339075327, 0.02706255898571250512, 0.02765076588687337758, 0.02823897278803425004, 0.02941538659035599496, 0.03059180039267773293, 0.03176821419499947785, 0.03235642109616034684, 0.03294462799732121583, 0.03412104179964296768, 0.03529745560196471260, 0.03647386940428645752, 0.03765028320660820244 ),
 .UNSPECIFIED. ) ;
#2229=CARTESIAN_POINT ( 'NONE',  ( 1.102718734937994105, -0.2049554913489460561, 0.9627163727494573164 ) ) ;
#2257=FACE_OUTER_BOUND ( 'NONE', #6587, .T. ) ;
#2263=CARTESIAN_POINT ( 'NONE',  ( 1.220472440944881942, -0.01566924555314537157, 0.9842519685039372579 ) ) ;
#2345=CARTESIAN_POINT ( 'NONE',  ( 0.7480314960629921295, 0.007724973897226917324, -0.9842519685039369248 ) ) ;
#2356=ORIENTED_EDGE ( 'NONE', *, *, #1670, .F. ) ;
#2359=CARTESIAN_POINT ( 'NONE',  ( 1.968503937007874072, 0.000000000000000000, 0.000000000000000000 ) ) ;
#2363=CARTESIAN_POINT ( 'NONE',  ( 0.8658672433185115036, -0.2045602151624222043, 0.9627673662903735163 ) ) ;
#2366=DIRECTION ( 'NONE',  ( 0.000000000000000000, 0.000000000000000000, -1.000000000000000000 ) ) ;
#2408=AXIS2_PLACEMENT_3D ( 'NONE', #5885, #646, #2967 ) ;
#2415=AXIS2_PLACEMENT_3D ( 'NONE', #6432, #4182, #4710 ) ;
#2418=EDGE_LOOP ( 'NONE', ( #2099, #623 ) ) ;
#2472=CARTESIAN_POINT ( 'NONE',  ( 1.220472440944881720, 1.984939871850715226E-17, -0.9842519685039370358 ) ) ;
#2481=DIRECTION ( 'NONE',  ( 0.000000000000000000, 0.000000000000000000, 1.000000000000000000 ) ) ;
#2521=EDGE_CURVE ( 'NONE', #1603, #4753, #230, .T. ) ;
#2556=AXIS2_PLACEMENT_3D ( 'NONE', #2954, #2878, #5295 ) ;
#2583=CARTESIAN_POINT ( 'NONE',  ( 1.015122112586412939, -0.2347042945180431994, -0.9558637132201285302 ) ) ;
#2623=CARTESIAN_POINT ( 'NONE',  ( 0.7719899816204534027, 0.1048018568659492278, -0.9787612993317383880 ) ) ;
#2647=CARTESIAN_POINT ( 'NONE',  ( 0.7495315129468413939, 0.03083906941738260785, 0.9838885550255186407 ) ) ;
#2657=CARTESIAN_POINT ( 'NONE',  ( 0.8062392625377295952, 0.1560493051692869171, -0.9718662726019896558 ) ) ;
#2658=AXIS2_PLACEMENT_3D ( 'NONE', #1201, #1777, #6413 ) ;
#2661=B_SPLINE_CURVE_WITH_KNOTS ( 'NONE', 3,
 ( #2472, #4808, #5427, #1860, #3160, #790, #1315, #5506, #1902, #2777, #2206, #417, #2740, #1461, #1544, #4468, #4537, #5081, #3351, #4386, #4427, #5625, #6871, #6756, #3387, #7398, #3970, #5703, #6298, #338, #1053, #5734, #1505, #2657, #3852, #6186, #2623, #375, #4960, #5044, #6332, #2845, #2345, #1764 ),
 .UNSPECIFIED., .F., .F.,
 ( 4, 2, 2, 2, 2, 2, 2, 2, 2, 2, 2, 2, 2, 2, 2, 2, 2, 2, 2, 2, 2, 4 ),
 ( 4.896973959386981381E-19, 0.001176728898091255592, 0.001765093347136882304, 0.002353457796182509016, 0.003530186694273764608, 0.004706915592365020634, 0.005883644490456278395, 0.007060373388547535288, 0.007648737837593169372, 0.008237102286638802590, 0.009413831184730070759, 0.01059056008282133893, 0.01176728898091260710, 0.01235565342995824031, 0.01294401787900387527, 0.01353238232804950848, 0.01412074677709514170, 0.01529747567518641160, 0.01647420457327768151, 0.01765093347136895141, 0.01823929792041458289, 0.01882766236946021784 ),
 .UNSPECIFIED. ) ;
#2683=ORIENTED_EDGE ( 'NONE', *, *, #4541, .T. ) ;
#2697=CARTESIAN_POINT ( 'NONE',  ( 0.8280287984149673486, -0.1778526427332735582, -0.9681128863842415333 ) ) ;
#2721=ORIENTED_EDGE ( 'NONE', *, *, #3984, .T. ) ;
#2734=ORIENTED_EDGE ( 'NONE', *, *, #1670, .T. ) ;
#2740=CARTESIAN_POINT ( 'NONE',  ( 1.128523761465410891, 0.1876879802734073011, -0.9662312300142489319 ) ) ;
#2741=DIRECTION ( 'NONE',  ( 1.000000000000000000, 0.000000000000000000, 0.000000000000000000 ) ) ;
#2768=DIMENSIONAL_EXPONENTS ( 1.000000000000000000, 0.000000000000000000, 0.000000000000000000, 0.000000000000000000, 0.000000000000000000, 0.000000000000000000, 0.000000000000000000 ) ;
#2777=CARTESIAN_POINT ( 'NONE',  ( 1.172031980416358365, 0.1441408498666779114, -0.9737261629585141076 ) ) ;
#2778=AXIS2_PLACEMENT_3D ( 'NONE', #6322, #6782, #1004 ) ;
#2805=ADVANCED_FACE ( 'NONE', ( #1292 ), #3637, .T. ) ;
#2815=AXIS2_PLACEMENT_3D ( 'NONE', #1971, #5954, #4186 ) ;
#2829=VERTEX_POINT ( 'NONE', #1611 ) ;
#2839=ORIENTED_EDGE ( 'NONE', *, *, #387, .F. ) ;
#2845=CARTESIAN_POINT ( 'NONE',  ( 0.7484094839556201251, 0.01546318525790828929, -0.9841610390795200169 ) ) ;
#2849=SHAPE_REPRESENTATION_RELATIONSHIP ( 'NONE' , 'NONE' ,  #2147, #3575 ) ;
#2869=CARTESIAN_POINT ( 'NONE',  ( 1.208238579388023037, 0.07659700195593643901, 0.9813707449069869471 ) ) ;
#2871=ORIENTED_EDGE ( 'NONE', *, *, #1028, .F. ) ;
#2878=DIRECTION ( 'NONE',  ( 1.000000000000000000, 0.000000000000000000, 0.000000000000000000 ) ) ;
#2916=CARTESIAN_POINT ( 'NONE',  ( 1.968503937007874072, 0.000000000000000000, 0.000000000000000000 ) ) ;
#2933=CARTESIAN_POINT ( 'NONE',  ( 1.038078147671274376, -0.2301377692397579833, 0.9569696942589730471 ) ) ;
#2934=EDGE_CURVE ( 'NONE', #6545, #1603, #2661, .T. ) ;
#2954=CARTESIAN_POINT ( 'NONE',  ( 1.968503937007874072, 0.000000000000000000, 0.000000000000000000 ) ) ;
#2967=DIRECTION ( 'NONE',  ( 0.000000000000000000, 0.000000000000000000, -1.000000000000000000 ) ) ;
#2987=EDGE_CURVE ( 'NONE', #3423, #4277, #3171, .T. ) ;
#2994=ORIENTED_EDGE ( 'NONE', *, *, #5635, .F. ) ;
#3004=APPLICATION_CONTEXT ( 'automotive_design' ) ;
#3054=DIRECTION ( 'NONE',  ( -1.000000000000000000, -0.000000000000000000, -0.000000000000000000 ) ) ;
#3072=( GEOMETRIC_REPRESENTATION_CONTEXT ( 3 ) GLOBAL_UNCERTAINTY_ASSIGNED_CONTEXT ( ( #3815 ) ) GLOBAL_UNIT_ASSIGNED_CONTEXT ( ( #1664, #6299, #5736 ) ) REPRESENTATION_CONTEXT ( 'NONE', 'WORKASPACE' ) );
#3105=LINE ( 'NONE', #926, #470 ) ;
#3119=CARTESIAN_POINT ( 'NONE',  ( 21.65354330708661479, 0.000000000000000000, 0.000000000000000000 ) ) ;
#3129=DIRECTION ( 'NONE',  ( 0.000000000000000000, 0.000000000000000000, 1.000000000000000000 ) ) ;
#3136=DIRECTION ( 'NONE',  ( 1.000000000000000000, 0.000000000000000000, 0.000000000000000000 ) ) ;
#3146=ORIENTED_EDGE ( 'NONE', *, *, #744, .F. ) ;
#3148=ORIENTED_EDGE ( 'NONE', *, *, #7505, .T. ) ;
#3160=CARTESIAN_POINT ( 'NONE',  ( 1.212519938569362798, 0.06127190455375051276, -0.9823712398279822455 ) ) ;
#3171=CIRCLE ( 'NONE', #2556, 0.9842519685039370358 ) ;
#3189=CARTESIAN_POINT ( 'NONE',  ( 0.7480314960629923515, 1.544184662414706467E-22, 0.9842519685039370358 ) ) ;
#3197=CARTESIAN_POINT ( 'NONE',  ( 1.218929327210600766, -0.03110856596261698734, -0.9838783093560928839 ) ) ;
#3238=CARTESIAN_POINT ( 'NONE',  ( 1.968503937007874072, 1.205361022782827973E-16, -0.9842519685039370358 ) ) ;
#3256=DIRECTION ( 'NONE',  ( -1.000000000000000000, -0.000000000000000000, -0.000000000000000000 ) ) ;
#3260=CARTESIAN_POINT ( 'NONE',  ( 1.060520566440911416, 0.2241008867759824719, 0.9584192624488059309 ) ) ;
#3267=DIRECTION ( 'NONE',  ( -1.000000000000000000, -0.000000000000000000, -0.000000000000000000 ) ) ;
#3268=CARTESIAN_POINT ( 'NONE',  ( 1.189145543181157505, -0.1185714375127665254, -0.9771702786582192601 ) ) ;
#3282=VECTOR ( 'NONE', #5308, 39.37007874015748143 ) ;
#3299=CARTESIAN_POINT ( 'NONE',  ( 1.089019577240956993, 0.2122777770860161672, 0.9611070884360988220 ) ) ;
#3313=AXIS2_PLACEMENT_3D ( 'NONE', #3119, #5466, #5586 ) ;
#3341=ORIENTED_EDGE ( 'NONE', *, *, #6825, .T. ) ;
#3351=CARTESIAN_POINT ( 'NONE',  ( 1.038078147671274376, 0.2301377692397579833, -0.9569696942589730471 ) ) ;
#3355=DIRECTION ( 'NONE',  ( 1.000000000000000000, 0.000000000000000000, 0.000000000000000000 ) ) ;
#3373=CARTESIAN_POINT ( 'NONE',  ( 0.9688787811271879491, -0.2362268424322147564, 0.9554835511204313736 ) ) ;
#3380=CARTESIAN_POINT ( 'NONE',  ( 1.128157436560226712, 0.1874853199515785218, 0.9662432197917761867 ) ) ;
#3387=CARTESIAN_POINT ( 'NONE',  ( 0.9080621969490132450, 0.2241341580870719608, -0.9584117186519856002 ) ) ;
#3411=CARTESIAN_POINT ( 'NONE',  ( 1.140380516255546706, -0.1779313096650642356, 0.9680979248264950376 ) ) ;
#3419=CARTESIAN_POINT ( 'NONE',  ( 1.218929327210600766, 0.03110856596261698734, 0.9838783093560928839 ) ) ;
#3423=VERTEX_POINT ( 'NONE', #3238 ) ;
#3432=FACE_BOUND ( 'NONE', #4461, .T. ) ;
#3454=ORIENTED_EDGE ( 'NONE', *, *, #2934, .F. ) ;
#3482=CARTESIAN_POINT ( 'NONE',  ( 1.060506290833840293, -0.2237082381425291866, 0.9584946220175588616 ) ) ;
#3490=PLANE ( 'NONE',  #1354 ) ;
#3507=CIRCLE ( 'NONE', #4724, 0.9842519685039370358 ) ;
#3510=ORIENTED_EDGE ( 'NONE', *, *, #744, .T. ) ;
#3553=EDGE_CURVE ( 'NONE', #2829, #10, #6713, .T. ) ;
#3575=ADVANCED_BREP_SHAPE_REPRESENTATION ( '', ( #1558, #5166 ), #3072 ) ;
#3636=CARTESIAN_POINT ( 'NONE',  ( 1.968503937007874072, 0.000000000000000000, 0.000000000000000000 ) ) ;
#3637=CYLINDRICAL_SURFACE ( 'NONE', #5129, 0.9842519685039370358 ) ;
#3660=CARTESIAN_POINT ( 'NONE',  ( 0.7723175066527832033, -0.1046133869837157365, -0.9787008116518934875 ) ) ;
#3689=DIRECTION ( 'NONE',  ( -0.000000000000000000, -0.000000000000000000, 1.000000000000000000 ) ) ;
#3718=CARTESIAN_POINT ( 'NONE',  ( 0.7480314960629921295, -0.007724973897226917324, 0.9842519685039369248 ) ) ;
#3731=CARTESIAN_POINT ( 'NONE',  ( 21.65354330708661479, 6.026805113914139867E-17, -0.4921259842519685179 ) ) ;
#3758=B_SPLINE_CURVE_WITH_KNOTS ( 'NONE', 3,
 ( #4056, #2263, #5788, #5140, #6282, #4021, #5243, #549, #7453, #2, #1071, #3411, #1134, #2229, #5208, #5751, #3482, #6994, #2933, #7157, #1041, #3373, #4598, #6895, #4089, #5275, #38, #2363, #1648, #4698, #1610, #3955, #517, #3992, #5180, #7490, #1288, #5896, #1372, #1330, #693, #5315, #3718, #1209 ),
 .UNSPECIFIED., .F., .F.,
 ( 4, 2, 2, 2, 2, 2, 2, 2, 2, 2, 2, 2, 2, 2, 2, 2, 2, 2, 2, 2, 2, 4 ),
 ( 4.896973959386981381E-19, 0.001176728898091255592, 0.001765093347136882304, 0.002353457796182509016, 0.003530186694273764608, 0.004706915592365020634, 0.005883644490456278395, 0.007060373388547535288, 0.007648737837593169372, 0.008237102286638802590, 0.009413831184730070759, 0.01059056008282133893, 0.01176728898091260710, 0.01235565342995824031, 0.01294401787900387527, 0.01353238232804950848, 0.01412074677709514170, 0.01529747567518641160, 0.01647420457327768151, 0.01765093347136895141, 0.01823929792041458289, 0.01882766236946021784 ),
 .UNSPECIFIED. ) ;
#3791=ORIENTED_EDGE ( 'NONE', *, *, #1537, .T. ) ;
#3798=ORIENTED_EDGE ( 'NONE', *, *, #2521, .T. ) ;
#3801=AXIS2_PLACEMENT_3D ( 'NONE', #2359, #1327, #5889 ) ;
#3815=UNCERTAINTY_MEASURE_WITH_UNIT (LENGTH_MEASURE( 1.000000000000000082E-05 ), #1664, 'distance_accuracy_value', 'NONE');
#3833=ORIENTED_EDGE ( 'NONE', *, *, #4541, .F. ) ;
#3844=CARTESIAN_POINT ( 'NONE',  ( 0.7480314960629922405, 0.01544581072159242723, 0.9842519685039369248 ) ) ;
#3850=CARTESIAN_POINT ( 'NONE',  ( 0.8656462225360395113, -0.2048623079342055120, -0.9627353284137957212 ) ) ;
#3852=CARTESIAN_POINT ( 'NONE',  ( 0.7965081100895167188, 0.1441822837186601813, -0.9737193899100770045 ) ) ;
#3859=ORIENTED_EDGE ( 'NONE', *, *, #5162, .T. ) ;
#3875=CARTESIAN_POINT ( 'NONE',  ( 0.8656462225360395113, 0.2048623079342055120, 0.9627353284137957212 ) ) ;
#3883=LINE ( 'NONE', #7354, #1506 ) ;
#3889=CARTESIAN_POINT ( 'NONE',  ( 1.220472440944882164, -0.01566504975835071242, -0.9842519685039374799 ) ) ;
#3899=ORIENTED_EDGE ( 'NONE', *, *, #891, .T. ) ;
#3904=DIRECTION ( 'NONE',  ( -1.000000000000000000, -0.000000000000000000, -0.000000000000000000 ) ) ;
#3914=DIRECTION ( 'NONE',  ( 1.000000000000000000, 0.000000000000000000, 0.000000000000000000 ) ) ;
#3955=CARTESIAN_POINT ( 'NONE',  ( 0.8284312913633176123, -0.1777059077220142780, 0.9680895064399986927 ) ) ;
#3958=FACE_OUTER_BOUND ( 'NONE', #5606, .T. ) ;
#3962=CARTESIAN_POINT ( 'NONE',  ( 1.162034203329631143, 0.1562967039942805003, 0.9718251695195749829 ) ) ;
#3970=CARTESIAN_POINT ( 'NONE',  ( 0.8794895096619267383, 0.2118599820681134061, -0.9611874069187010816 ) ) ;
#3978=EDGE_CURVE ( 'NONE', #4277, #6588, #3105, .T. ) ;
#3983=CARTESIAN_POINT ( 'NONE',  ( 1.968503937007874072, 0.000000000000000000, 0.000000000000000000 ) ) ;
#3984=EDGE_CURVE ( 'NONE', #1603, #4456, #1450, .T. ) ;
#3992=CARTESIAN_POINT ( 'NONE',  ( 0.8062392625377295952, -0.1560493051692869171, 0.9718662726019896558 ) ) ;
#4021=CARTESIAN_POINT ( 'NONE',  ( 1.207998888640173130, -0.07614347099379424610, 0.9813305615101511892 ) ) ;
#4041=DIRECTION ( 'NONE',  ( 1.000000000000000000, 0.000000000000000000, 0.000000000000000000 ) ) ;
#4051=LINE ( 'NONE', #7113, #1861 ) ;
#4056=CARTESIAN_POINT ( 'NONE',  ( 1.220472440944881720, -1.984939871850715226E-17, 0.9842519685039370358 ) ) ;
#4066=ADVANCED_FACE ( 'NONE', ( #3958 ), #7267, .F. ) ;
#4089=CARTESIAN_POINT ( 'NONE',  ( 0.9080621969490132450, -0.2241341580870719608, 0.9584117186519856002 ) ) ;
#4182=DIRECTION ( 'NONE',  ( 1.000000000000000000, 0.000000000000000000, 0.000000000000000000 ) ) ;
#4186=DIRECTION ( 'NONE',  ( 1.000000000000000000, 0.000000000000000000, 0.000000000000000000 ) ) ;
#4230=CARTESIAN_POINT ( 'NONE',  ( 0.7690174846032691303, -0.09763972085202782258, -0.9794230103293317669 ) ) ;
#4256=EDGE_CURVE ( 'NONE', #4277, #3423, #3507, .T. ) ;
#4277=VERTEX_POINT ( 'NONE', #731 ) ;
#4297=CARTESIAN_POINT ( 'NONE',  ( 0.9227869198894881331, 0.2286038407206694989, 0.9573410596537438311 ) ) ;
#4340=CARTESIAN_POINT ( 'NONE',  ( 0.8401230830384029957, 0.1877837920673497696, 0.9662117393330279524 ) ) ;
#4346=CARTESIAN_POINT ( 'NONE',  ( 1.220472440944881720, 1.984939871850715226E-17, -0.9842519685039370358 ) ) ;
#4352=CARTESIAN_POINT ( 'NONE',  ( 0.000000000000000000, 1.205361022782827973E-16, -0.9842519685039370358 ) ) ;
#4360=CARTESIAN_POINT ( 'NONE',  ( 1.968503937007874072, 0.000000000000000000, 0.4921259842519685179 ) ) ;
#4383=CARTESIAN_POINT ( 'NONE',  ( 0.9997522001112967294, -0.2362259618796917759, -0.9554837688155867204 ) ) ;
#4386=CARTESIAN_POINT ( 'NONE',  ( 1.015186846506429985, 0.2347025779575657722, -0.9558642380754210910 ) ) ;
#4412=CARTESIAN_POINT ( 'NONE',  ( 0.9079010304997725544, 0.2240813082648737964, 0.9584242268600799974 ) ) ;
#4423=CARTESIAN_POINT ( 'NONE',  ( 0.7836514762968587178, -0.1249763776241986785, -0.9763066675542205752 ) ) ;
#4427=CARTESIAN_POINT ( 'NONE',  ( 0.9998202959290236613, 0.2362140621487221481, -0.9554867107345892396 ) ) ;
#4437=APPLICATION_CONTEXT ( 'automotive_design' ) ;
#4451=AXIS2_PLACEMENT_3D ( 'NONE', #2916, #3355, #25 ) ;
#4456=VERTEX_POINT ( 'NONE', #5020 ) ;
#4461=EDGE_LOOP ( 'NONE', ( #1609, #2356 ) ) ;
#4468=CARTESIAN_POINT ( 'NONE',  ( 1.067758866085110281, 0.2211013871911202966, -0.9591012775692122627 ) ) ;
#4515=DIRECTION ( 'NONE',  ( 0.000000000000000000, 0.000000000000000000, -1.000000000000000000 ) ) ;
#4535=( NAMED_UNIT ( * ) PLANE_ANGLE_UNIT ( ) SI_UNIT ( $, .RADIAN. ) );
#4537=CARTESIAN_POINT ( 'NONE',  ( 1.060506290833840293, 0.2237082381425291866, -0.9584946220175588616 ) ) ;
#4541=EDGE_CURVE ( 'NONE', #2119, #2829, #590, .T. ) ;
#4575=( CONVERSION_BASED_UNIT ( 'INCH', #4641 ) LENGTH_UNIT ( ) NAMED_UNIT ( #436 ) );
#4579=LENGTH_MEASURE_WITH_UNIT ( LENGTH_MEASURE( 0.02539999999999999897 ), #458 );
#4598=CARTESIAN_POINT ( 'NONE',  ( 0.9531588649300888338, -0.2346757028646479781, 0.9558707923556580832 ) ) ;
#4612=FACE_OUTER_BOUND ( 'NONE', #297, .T. ) ;
#4625=EDGE_CURVE ( 'NONE', #4753, #6362, #1682, .T. ) ;
#4641=LENGTH_MEASURE_WITH_UNIT ( LENGTH_MEASURE( 0.02539999999999999897 ), #455 );
#4698=CARTESIAN_POINT ( 'NONE',  ( 0.8465112843344620996, -0.1920587529112295633, 0.9653415754825105388 ) ) ;
#4710=DIRECTION ( 'NONE',  ( 0.000000000000000000, 0.000000000000000000, -1.000000000000000000 ) ) ;
#4724=AXIS2_PLACEMENT_3D ( 'NONE', #3636, #1291, #2366 ) ;
#4729=DIRECTION ( 'NONE',  ( -1.000000000000000000, -0.000000000000000000, -0.000000000000000000 ) ) ;
#4753=VERTEX_POINT ( 'NONE', #4352 ) ;
#4763=DIRECTION ( 'NONE',  ( -1.000000000000000000, -0.000000000000000000, -0.000000000000000000 ) ) ;
#4806=CARTESIAN_POINT ( 'NONE',  ( 0.7480314960629922405, -0.01544581072159242723, -0.9842519685039369248 ) ) ;
#4808=CARTESIAN_POINT ( 'NONE',  ( 1.220472440944881942, 0.01566924555314537157, -0.9842519685039372579 ) ) ;
#4876=FACE_OUTER_BOUND ( 'NONE', #1039, .T. ) ;
#4906=CARTESIAN_POINT ( 'NONE',  ( 0.7480314960629923515, 2.892866454678784449E-17, -1.377952755905512028 ) ) ;
#4915=AXIS2_PLACEMENT_3D ( 'NONE', #1122, #6336, #3129 ) ;
#4921=CARTESIAN_POINT ( 'NONE',  ( 1.140074190135267118, -0.1777047106289595946, -0.9680897379949867654 ) ) ;
#4945=MECHANICAL_DESIGN_GEOMETRIC_PRESENTATION_REPRESENTATION('',(#5694),#296);
#4960=CARTESIAN_POINT ( 'NONE',  ( 0.7556634140584972403, 0.06154568813258620014, -0.9824437959648022467 ) ) ;
#4963=ADVANCED_FACE ( 'NONE', ( #6982 ), #538, .F. ) ;
#4989=CARTESIAN_POINT ( 'NONE',  ( 0.9530933633567026941, 0.2342849080887553226, 0.9559618965236083010 ) ) ;
#5002=ADVANCED_FACE ( 'NONE', ( #4612 ), #599, .T. ) ;
#5020=CARTESIAN_POINT ( 'NONE',  ( 0.7480314960629923515, 1.544184662414706467E-22, 0.9842519685039370358 ) ) ;
#5044=CARTESIAN_POINT ( 'NONE',  ( 0.7511002112796222319, 0.03873617871155973086, -0.9835188775901014813 ) ) ;
#5079=CARTESIAN_POINT ( 'NONE',  ( 0.7480314960629923515, 1.205359478595430764E-16, -0.9842519685039370358 ) ) ;
#5081=CARTESIAN_POINT ( 'NONE',  ( 1.045688647185073705, 0.2282227683634086846, -0.9574297281001666882 ) ) ;
#5102=ORIENTED_EDGE ( 'NONE', *, *, #4256, .F. ) ;
#5116=EDGE_CURVE ( 'NONE', #2119, #1248, #820, .T. ) ;
#5129=AXIS2_PLACEMENT_3D ( 'NONE', #732, #3054, #5404 ) ;
#5140=CARTESIAN_POINT ( 'NONE',  ( 1.214400861842334090, -0.05376942629958520597, 0.9828113691670130603 ) ) ;
#5162=EDGE_CURVE ( 'NONE', #4456, #6588, #191, .T. ) ;
#5166=AXIS2_PLACEMENT_3D ( 'NONE', #418, #2134, #2741 ) ;
#5180=CARTESIAN_POINT ( 'NONE',  ( 0.7965081100895167188, -0.1441822837186601813, 0.9737193899100770045 ) ) ;
#5208=CARTESIAN_POINT ( 'NONE',  ( 1.089060247968624440, -0.2122540722833457794, 0.9611122372014845316 ) ) ;
#5212=CARTESIAN_POINT ( 'NONE',  ( 1.212838072735738848, 0.06155971505712520137, 0.9824432156515408021 ) ) ;
#5243=CARTESIAN_POINT ( 'NONE',  ( 1.205350347085700102, -0.08351947907094880996, 0.9807282671443031674 ) ) ;
#5275=CARTESIAN_POINT ( 'NONE',  ( 0.8865586066401955900, -0.2152123167378564572, 0.9604399500593175931 ) ) ;
#5295=DIRECTION ( 'NONE',  ( 0.000000000000000000, 0.000000000000000000, -1.000000000000000000 ) ) ;
#5308=DIRECTION ( 'NONE',  ( -1.000000000000000000, -0.000000000000000000, -0.000000000000000000 ) ) ;
#5315=CARTESIAN_POINT ( 'NONE',  ( 0.7484094839556201251, -0.01546318525790828929, 0.9841610390795200169 ) ) ;
#5354=EDGE_LOOP ( 'NONE', ( #2839, #5102, #1766, #1148, #2187, #3899, #6710, #3791 ) ) ;
#5404=DIRECTION ( 'NONE',  ( 0.000000000000000000, 0.000000000000000000, 1.000000000000000000 ) ) ;
#5415=PRODUCT_CONTEXT ( 'NONE', #4437, 'mechanical' ) ;
#5425=CARTESIAN_POINT ( 'NONE',  ( 0.7796304418040825857, -0.1182802082656420201, -0.9771433015668254951 ) ) ;
#5427=CARTESIAN_POINT ( 'NONE',  ( 1.218928898036171882, 0.03106543388645563800, -0.9838782854499440456 ) ) ;
#5442=ORIENTED_EDGE ( 'NONE', *, *, #3984, .F. ) ;
#5455=ORIENTED_EDGE ( 'NONE', *, *, #4256, .T. ) ;
#5466=DIRECTION ( 'NONE',  ( 1.000000000000000000, 0.000000000000000000, 0.000000000000000000 ) ) ;
#5471=CARTESIAN_POINT ( 'NONE',  ( 1.968503937007874072, 1.205361022782827973E-16, -0.9842519685039370358 ) ) ;
#5506=CARTESIAN_POINT ( 'NONE',  ( 1.196439825128248202, 0.1049569639594290504, -0.9787451009560118598 ) ) ;
#5539=CARTESIAN_POINT ( 'NONE',  ( 0.7723175066527832033, 0.1046133869837157365, 0.9787008116518934875 ) ) ;
#5582=CARTESIAN_POINT ( 'NONE',  ( 1.128157436560226712, -0.1874853199515785218, -0.9662432197917761867 ) ) ;
#5586=DIRECTION ( 'NONE',  ( 0.000000000000000000, 0.000000000000000000, -1.000000000000000000 ) ) ;
#5606=EDGE_LOOP ( 'NONE', ( #5442, #3454, #3510, #7377 ) ) ;
#5620=CARTESIAN_POINT ( 'NONE',  ( 1.208238579388023037, -0.07659700195593643901, -0.9813707449069869471 ) ) ;
#5625=CARTESIAN_POINT ( 'NONE',  ( 0.9688787811271879491, 0.2362268424322147564, -0.9554835511204313736 ) ) ;
#5635=EDGE_CURVE ( 'NONE', #4456, #6362, #4051, .T. ) ;
#5650=CARTESIAN_POINT ( 'NONE',  ( 1.102581283201567564, 0.2050316615124324060, 0.9626998336838916703 ) ) ;
#5694=STYLED_ITEM('',(#7587),#1558);
#5703=CARTESIAN_POINT ( 'NONE',  ( 0.8658672433185115036, 0.2045602151624222043, -0.9627673662903735163 ) ) ;
#5734=CARTESIAN_POINT ( 'NONE',  ( 0.8284312913633176123, 0.1777059077220142780, -0.9680895064399986927 ) ) ;
#5736=( NAMED_UNIT ( * ) SI_UNIT ( $, .STERADIAN. ) SOLID_ANGLE_UNIT ( ) );
#5751=CARTESIAN_POINT ( 'NONE',  ( 1.067758866085110281, -0.2211013871911202966, 0.9591012775692122627 ) ) ;
#5763=CIRCLE ( 'NONE', #3801, 0.4921259842519685179 ) ;
#5788=CARTESIAN_POINT ( 'NONE',  ( 1.218928898036171882, -0.03106543388645563800, 0.9838782854499440456 ) ) ;
#5806=CARTESIAN_POINT ( 'NONE',  ( 0.000000000000000000, 0.000000000000000000, 0.000000000000000000 ) ) ;
#5827=EDGE_LOOP ( 'NONE', ( #5455, #6019 ) ) ;
#5833=ORIENTED_EDGE ( 'NONE', *, *, #3553, .F. ) ;
#5862=VECTOR ( 'NONE', #3267, 39.37007874015748143 ) ;
#5885=CARTESIAN_POINT ( 'NONE',  ( 0.000000000000000000, 0.000000000000000000, 0.000000000000000000 ) ) ;
#5889=DIRECTION ( 'NONE',  ( 0.000000000000000000, 0.000000000000000000, -1.000000000000000000 ) ) ;
#5896=CARTESIAN_POINT ( 'NONE',  ( 0.7601524118086268045, -0.07627561187719542057, 0.9813965260305658189 ) ) ;
#5954=DIRECTION ( 'NONE',  ( -0.000000000000000000, -0.000000000000000000, 1.000000000000000000 ) ) ;
#5961=PRODUCT_DEFINITION_CONTEXT ( 'detailed design', #3004, 'design' ) ;
#5984=CARTESIAN_POINT ( 'NONE',  ( 1.220472440944881720, 0.000000000000000000, -1.377952755905512028 ) ) ;
#6019=ORIENTED_EDGE ( 'NONE', *, *, #2987, .T. ) ;
#6068=CARTESIAN_POINT ( 'NONE',  ( 0.7556465724085326130, 0.06151677279835152806, 0.9824476696380366469 ) ) ;
#6074=CARTESIAN_POINT ( 'NONE',  ( 0.7965271477292853453, -0.1442139612367993318, -0.9737154292565876057 ) ) ;
#6103=ORIENTED_EDGE ( 'NONE', *, *, #4625, .T. ) ;
#6108=CARTESIAN_POINT ( 'NONE',  ( 1.121892893784558254, -0.1921327968434894951, -0.9653269806155788668 ) ) ;
#6144=VECTOR ( 'NONE', #4763, 39.37007874015748143 ) ;
#6149=CARTESIAN_POINT ( 'NONE',  ( 1.089019577240956993, -0.2122777770860161672, -0.9611070884360988220 ) ) ;
#6175=CARTESIAN_POINT ( 'NONE',  ( 1.015122112586412939, 0.2347042945180431994, 0.9558637132201285302 ) ) ;
#6183=CARTESIAN_POINT ( 'NONE',  ( 1.060520566440911416, -0.2241008867759824719, -0.9584192624488059309 ) ) ;
#6186=CARTESIAN_POINT ( 'NONE',  ( 0.7794093496269024479, 0.1186414295356391785, -0.9771602695683655471 ) ) ;
#6203=VECTOR ( 'NONE', #3689, 39.37007874015748143 ) ;
#6261=CARTESIAN_POINT ( 'NONE',  ( 0.000000000000000000, 0.000000000000000000, 0.9842519685039370358 ) ) ;
#6282=CARTESIAN_POINT ( 'NONE',  ( 1.212519938569362798, -0.06127190455375051276, 0.9823712398279822455 ) ) ;
#6298=CARTESIAN_POINT ( 'NONE',  ( 0.8592737258235019215, 0.2005978551774719454, -0.9636033532647499955 ) ) ;
#6299=( NAMED_UNIT ( * ) PLANE_ANGLE_UNIT ( ) SI_UNIT ( $, .RADIAN. ) );
#6322=CARTESIAN_POINT ( 'NONE',  ( 0.9842519685039370358, 0.000000000000000000, -1.377952755905512028 ) ) ;
#6326=CARTESIAN_POINT ( 'NONE',  ( 1.220472440944882164, 0.01566504975835071242, 0.9842519685039374799 ) ) ;
#6332=CARTESIAN_POINT ( 'NONE',  ( 0.7499405322945513763, 0.03096673178975459240, -0.9837952645051013523 ) ) ;
#6336=DIRECTION ( 'NONE',  ( -1.000000000000000000, -0.000000000000000000, -0.000000000000000000 ) ) ;
#6341=CYLINDRICAL_SURFACE ( 'NONE', #6859, 0.9842519685039370358 ) ;
#6358=CARTESIAN_POINT ( 'NONE',  ( 1.145762533245342940, 0.1725491722722915233, 0.9690247371578599722 ) ) ;
#6362=VERTEX_POINT ( 'NONE', #6261 ) ;
#6413=DIRECTION ( 'NONE',  ( 0.000000000000000000, 0.000000000000000000, -1.000000000000000000 ) ) ;
#6432=CARTESIAN_POINT ( 'NONE',  ( 1.968503937007874072, 0.000000000000000000, 0.000000000000000000 ) ) ;
#6545=VERTEX_POINT ( 'NONE', #7127 ) ;
#6547=FACE_OUTER_BOUND ( 'NONE', #491, .T. ) ;
#6565=CARTESIAN_POINT ( 'NONE',  ( 1.220472440944881720, -1.984939871850715226E-17, 0.9842519685039370358 ) ) ;
#6582=CIRCLE ( 'NONE', #2415, 0.4921259842519685179 ) ;
#6587=EDGE_LOOP ( 'NONE', ( #2078, #927, #7415, #3798, #6103, #2994, #3859, #2010 ) ) ;
#6588=VERTEX_POINT ( 'NONE', #6565 ) ;
#6598=ADVANCED_FACE ( 'NONE', ( #4876 ), #2012, .F. ) ;
#6611=CIRCLE ( 'NONE', #3313, 0.4921259842519685179 ) ;
#6636=CARTESIAN_POINT ( 'NONE',  ( 1.121892893784558254, 0.1921327968434894951, 0.9653269806155788668 ) ) ;
#6642=CARTESIAN_POINT ( 'NONE',  ( 1.212838072735738848, -0.06155971505712520137, -0.9824432156515408021 ) ) ;
#6650=CYLINDRICAL_SURFACE ( 'NONE', #720, 0.4921259842519685179 ) ;
#6707=ORIENTED_EDGE ( 'NONE', *, *, #5116, .F. ) ;
#6708=CARTESIAN_POINT ( 'NONE',  ( 0.7796304418040825857, 0.1182802082656420201, 0.9771433015668254951 ) ) ;
#6710=ORIENTED_EDGE ( 'NONE', *, *, #2521, .F. ) ;
#6713=LINE ( 'NONE', #372, #5862 ) ;
#6714=CARTESIAN_POINT ( 'NONE',  ( 0.9454567723360981502, -0.2331403729576253803, -0.9562426076827387211 ) ) ;
#6752=CARTESIAN_POINT ( 'NONE',  ( 1.196402575039207328, -0.1050201062211118808, -0.9787371541722721391 ) ) ;
#6756=CARTESIAN_POINT ( 'NONE',  ( 0.9228159122846772977, 0.2286155672763659219, -0.9573382785580841770 ) ) ;
#6782=DIRECTION ( 'NONE',  ( -0.000000000000000000, -0.000000000000000000, 1.000000000000000000 ) ) ;
#6795=CARTESIAN_POINT ( 'NONE',  ( 0.8401230830384029957, -0.1877837920673497696, -0.9662117393330279524 ) ) ;
#6813=CARTESIAN_POINT ( 'NONE',  ( 0.000000000000000000, 0.000000000000000000, 0.000000000000000000 ) ) ;
#6825=EDGE_CURVE ( 'NONE', #10, #1248, #5763, .T. ) ;
#6833=( NAMED_UNIT ( * ) SI_UNIT ( $, .STERADIAN. ) SOLID_ANGLE_UNIT ( ) );
#6844=DIRECTION ( 'NONE',  ( 0.000000000000000000, 0.000000000000000000, 1.000000000000000000 ) ) ;
#6859=AXIS2_PLACEMENT_3D ( 'NONE', #3983, #3904, #6844 ) ;
#6871=CARTESIAN_POINT ( 'NONE',  ( 0.9531588649300888338, 0.2346757028646479781, -0.9558707923556580832 ) ) ;
#6895=CARTESIAN_POINT ( 'NONE',  ( 0.9228159122846772977, -0.2286155672763659219, 0.9573382785580841770 ) ) ;
#6932=CARTESIAN_POINT ( 'NONE',  ( 1.189145543181157505, 0.1185714375127665254, 0.9771702786582192601 ) ) ;
#6982=FACE_OUTER_BOUND ( 'NONE', #2418, .T. ) ;
#6985=AXIS2_PLACEMENT_3D ( 'NONE', #5806, #4041, #1151 ) ;
#6994=CARTESIAN_POINT ( 'NONE',  ( 1.045688647185073705, -0.2282227683634086846, 0.9574297281001666882 ) ) ;
#7113=CARTESIAN_POINT ( 'NONE',  ( 1.968503937007874072, 0.000000000000000000, 0.9842519685039370358 ) ) ;
#7127=CARTESIAN_POINT ( 'NONE',  ( 1.220472440944881720, 1.984939871850715226E-17, -0.9842519685039370358 ) ) ;
#7132=CARTESIAN_POINT ( 'NONE',  ( 0.7495315129468413939, -0.03083906941738260785, -0.9838885550255186407 ) ) ;
#7140=EDGE_LOOP ( 'NONE', ( #3833, #120, #2734, #5833 ) ) ;
#7157=CARTESIAN_POINT ( 'NONE',  ( 1.015186846506429985, -0.2347025779575657722, 0.9558642380754210910 ) ) ;
#7166=CARTESIAN_POINT ( 'NONE',  ( 0.7556465724085326130, -0.06151677279835152806, -0.9824476696380366469 ) ) ;
#7193=ADVANCED_FACE ( 'NONE', ( #2257 ), #6341, .T. ) ;
#7196=CARTESIAN_POINT ( 'NONE',  ( 0.7965271477292853453, 0.1442139612367993318, 0.9737154292565876057 ) ) ;
#7203=CARTESIAN_POINT ( 'NONE',  ( 0.8062609481994166272, -0.1560654929534785462, -0.9718629971449804783 ) ) ;
#7218=ORIENTED_EDGE ( 'NONE', *, *, #7505, .F. ) ;
#7236=CARTESIAN_POINT ( 'NONE',  ( 0.7601650273709252836, 0.07630400123961592063, 0.9813937435533869325 ) ) ;
#7247=CARTESIAN_POINT ( 'NONE',  ( 1.171887040486664588, -0.1443386382778019672, -0.9736977440596933375 ) ) ;
#7267=CYLINDRICAL_SURFACE ( 'NONE', #2778, 0.2362204724409446843 ) ;
#7278=CARTESIAN_POINT ( 'NONE',  ( 1.162034203329631143, -0.1562967039942805003, -0.9718251695195749829 ) ) ;
#7308=CARTESIAN_POINT ( 'NONE',  ( 0.9685300475558180633, 0.2358242948353262147, 0.9555833128140062138 ) ) ;
#7354=CARTESIAN_POINT ( 'NONE',  ( 1.968503937007874072, 1.205361022782827973E-16, -0.9842519685039370358 ) ) ;
#7357=CARTESIAN_POINT ( 'NONE',  ( 1.045446081760740942, -0.2286795840550674142, -0.9573229298165720769 ) ) ;
#7369=CLOSED_SHELL ( 'NONE', ( #2168, #6598, #7193, #2805, #1425, #4963, #4066, #5002, #1189 ) ) ;
#7377=ORIENTED_EDGE ( 'NONE', *, *, #5162, .F. ) ;
#7398=CARTESIAN_POINT ( 'NONE',  ( 0.8865586066401955900, 0.2152123167378564572, -0.9604399500593175931 ) ) ;
#7415=ORIENTED_EDGE ( 'NONE', *, *, #2934, .T. ) ;
#7437=PLANE ( 'NONE',  #4451 ) ;
#7453=CARTESIAN_POINT ( 'NONE',  ( 1.189177986357916605, -0.1185041968903534776, 0.9771775582510943137 ) ) ;
#7466=CIRCLE ( 'NONE', #1853, 0.9842519685039370358 ) ;
#7477=UNCERTAINTY_MEASURE_WITH_UNIT (LENGTH_MEASURE( 1.000000000000000082E-05 ), #4575, 'distance_accuracy_value', 'NONE');
#7490=CARTESIAN_POINT ( 'NONE',  ( 0.7794093496269024479, -0.1186414295356391785, 0.9771602695683655471 ) ) ;
#7494=CARTESIAN_POINT ( 'NONE',  ( 1.196402575039207328, 0.1050201062211118808, 0.9787371541722721391 ) ) ;
#7505=EDGE_CURVE ( 'NONE', #2829, #2119, #6611, .T. ) ;
#7581=COLOUR_RGB('Black',0.12,0.14,0.17);
#7582=FILL_AREA_STYLE_COLOUR('',#7581);
#7583=FILL_AREA_STYLE('',(#7582));
#7584=SURFACE_STYLE_FILL_AREA(#7583);
#7585=SURFACE_SIDE_STYLE('',(#7584));
#7586=SURFACE_STYLE_USAGE(.BOTH.,#7585);
#7587=PRESENTATION_STYLE_ASSIGNMENT((#7586));
ENDSEC;
END-ISO-10303-21;
